ISO-10303-21;
HEADER;
/* Generated by software containing ST-Developer
 * from STEP Tools, Inc. (www.steptools.com) 
 */

FILE_DESCRIPTION(
/* description */ ('CAx-IF Rec.Pracs.---Representation and Presentation of Product Manufa
cturing Information (PMI)---4.0---2014-10-13'),
/* implementation_level */ '2;1');

FILE_NAME(
/* name */ 'Socket Screw 4.step',
/* time_stamp */ '2026-10-24T18:52:33-07:00',
/* author */ (''),
/* organization */ (''),
/* preprocessor_version */ 'ST-DEVELOPER v20.2',
/* originating_system */ 'Autodesk Translation Framework v15.17.0.0',
/* authorisation */ '');

FILE_SCHEMA (('AP242_MANAGED_MODEL_BASED_3D_ENGINEERING_MIM_LF { 1 0 10303 442 2 1 4 }'));
ENDSEC;

DATA;
#10=MECHANICAL_DESIGN_GEOMETRIC_PRESENTATION_REPRESENTATION('',(#433),#34876);
#367=SHAPE_REPRESENTATION_RELATIONSHIP('SRR','None',#35004,#400);
#400=ADVANCED_BREP_SHAPE_REPRESENTATION('',(#466),#34862);
#433=STYLED_ITEM('',(#35166),#466);
#466=MANIFOLD_SOLID_BREP('Socket Screw 4',#19573);
#917=PLANE('',#21363);
#918=PLANE('',#21364);
#919=PLANE('',#21365);
#920=PLANE('',#21369);
#921=PLANE('',#21370);
#922=PLANE('',#21371);
#923=PLANE('',#21372);
#924=PLANE('',#21373);
#2064=LINE('',#32339,#3663);
#2065=LINE('',#32341,#3664);
#2066=LINE('',#32343,#3665);
#2067=LINE('',#32344,#3666);
#2068=LINE('',#32347,#3667);
#2069=LINE('',#32349,#3668);
#2070=LINE('',#32350,#3669);
#2071=LINE('',#32353,#3670);
#2072=LINE('',#32357,#3671);
#2073=LINE('',#32359,#3672);
#2074=LINE('',#32360,#3673);
#2075=LINE('',#32363,#3674);
#2076=LINE('',#32365,#3675);
#2077=LINE('',#32368,#3676);
#2078=LINE('',#32370,#3677);
#2079=LINE('',#32372,#3678);
#2080=LINE('',#32373,#3679);
#2081=LINE('',#32376,#3680);
#2082=LINE('',#32378,#3681);
#3663=VECTOR('',#26065,1.);
#3664=VECTOR('',#26066,1.);
#3665=VECTOR('',#26067,1.);
#3666=VECTOR('',#26068,1.);
#3667=VECTOR('',#26071,1.);
#3668=VECTOR('',#26072,1.);
#3669=VECTOR('',#26073,1.);
#3670=VECTOR('',#26076,1.);
#3671=VECTOR('',#26079,1.);
#3672=VECTOR('',#26080,1.);
#3673=VECTOR('',#26081,1.);
#3674=VECTOR('',#26084,1.);
#3675=VECTOR('',#26085,1.);
#3676=VECTOR('',#26090,1.);
#3677=VECTOR('',#26091,1.);
#3678=VECTOR('',#26092,1.);
#3679=VECTOR('',#26093,1.);
#3680=VECTOR('',#26098,1.);
#3681=VECTOR('',#26101,1.);
#4587=CYLINDRICAL_SURFACE('',#21367,0.0005);
#5444=FACE_OUTER_BOUND('',#6567,.T.);
#5445=FACE_OUTER_BOUND('',#6568,.T.);
#5446=FACE_OUTER_BOUND('',#6569,.T.);
#5447=FACE_OUTER_BOUND('',#6570,.T.);
#5448=FACE_OUTER_BOUND('',#6571,.T.);
#5449=FACE_OUTER_BOUND('',#6572,.T.);
#5450=FACE_OUTER_BOUND('',#6573,.T.);
#5451=FACE_OUTER_BOUND('',#6574,.T.);
#5452=FACE_OUTER_BOUND('',#6575,.T.);
#6567=EDGE_LOOP('',(#16292,#16293,#16294,#16295));
#6568=EDGE_LOOP('',(#16296,#16297,#16298,#16299));
#6569=EDGE_LOOP('',(#16300,#16301,#16302,#16303,#16304,#16305,#16306));
#6570=EDGE_LOOP('',(#16307,#16308,#16309,#16310));
#6571=EDGE_LOOP('',(#16311,#16312,#16313,#16314,#16315,#16316,#16317));
#6572=EDGE_LOOP('',(#16318,#16319,#16320,#16321));
#6573=EDGE_LOOP('',(#16322,#16323,#16324,#16325));
#6574=EDGE_LOOP('',(#16326,#16327,#16328,#16329));
#6575=EDGE_LOOP('',(#16330,#16331,#16332,#16333));
#7621=CIRCLE('',#21366,0.00050000000001);
#7622=CIRCLE('',#21368,0.00050000000001);
#9227=VERTEX_POINT('',#32337);
#9228=VERTEX_POINT('',#32338);
#9229=VERTEX_POINT('',#32340);
#9230=VERTEX_POINT('',#32342);
#9231=VERTEX_POINT('',#32346);
#9232=VERTEX_POINT('',#32348);
#9233=VERTEX_POINT('',#32352);
#9234=VERTEX_POINT('',#32354);
#9235=VERTEX_POINT('',#32356);
#9236=VERTEX_POINT('',#32358);
#9237=VERTEX_POINT('',#32362);
#9238=VERTEX_POINT('',#32364);
#9239=VERTEX_POINT('',#32369);
#9240=VERTEX_POINT('',#32371);
#11704=EDGE_CURVE('',#9227,#9228,#2064,.T.);
#11705=EDGE_CURVE('',#9228,#9229,#2065,.T.);
#11706=EDGE_CURVE('',#9229,#9230,#2066,.T.);
#11707=EDGE_CURVE('',#9227,#9230,#2067,.T.);
#11708=EDGE_CURVE('',#9231,#9229,#2068,.T.);
#11709=EDGE_CURVE('',#9232,#9231,#2069,.T.);
#11710=EDGE_CURVE('',#9230,#9232,#2070,.T.);
#11711=EDGE_CURVE('',#9233,#9232,#2071,.T.);
#11712=EDGE_CURVE('',#9234,#9233,#7621,.T.);
#11713=EDGE_CURVE('',#9234,#9235,#2072,.T.);
#11714=EDGE_CURVE('',#9236,#9235,#2073,.T.);
#11715=EDGE_CURVE('',#9236,#9227,#2074,.T.);
#11716=EDGE_CURVE('',#9234,#9237,#2075,.T.);
#11717=EDGE_CURVE('',#9233,#9238,#2076,.T.);
#11718=EDGE_CURVE('',#9237,#9238,#7622,.T.);
#11719=EDGE_CURVE('',#9238,#9231,#2077,.T.);
#11720=EDGE_CURVE('',#9228,#9239,#2078,.T.);
#11721=EDGE_CURVE('',#9240,#9239,#2079,.T.);
#11722=EDGE_CURVE('',#9237,#9240,#2080,.T.);
#11723=EDGE_CURVE('',#9239,#9236,#2081,.T.);
#11724=EDGE_CURVE('',#9235,#9240,#2082,.T.);
#16292=ORIENTED_EDGE('',*,*,#11704,.T.);
#16293=ORIENTED_EDGE('',*,*,#11705,.T.);
#16294=ORIENTED_EDGE('',*,*,#11706,.T.);
#16295=ORIENTED_EDGE('',*,*,#11707,.F.);
#16296=ORIENTED_EDGE('',*,*,#11706,.F.);
#16297=ORIENTED_EDGE('',*,*,#11708,.F.);
#16298=ORIENTED_EDGE('',*,*,#11709,.F.);
#16299=ORIENTED_EDGE('',*,*,#11710,.F.);
#16300=ORIENTED_EDGE('',*,*,#11707,.T.);
#16301=ORIENTED_EDGE('',*,*,#11710,.T.);
#16302=ORIENTED_EDGE('',*,*,#11711,.F.);
#16303=ORIENTED_EDGE('',*,*,#11712,.F.);
#16304=ORIENTED_EDGE('',*,*,#11713,.T.);
#16305=ORIENTED_EDGE('',*,*,#11714,.F.);
#16306=ORIENTED_EDGE('',*,*,#11715,.T.);
#16307=ORIENTED_EDGE('',*,*,#11716,.F.);
#16308=ORIENTED_EDGE('',*,*,#11712,.T.);
#16309=ORIENTED_EDGE('',*,*,#11717,.T.);
#16310=ORIENTED_EDGE('',*,*,#11718,.F.);
#16311=ORIENTED_EDGE('',*,*,#11718,.T.);
#16312=ORIENTED_EDGE('',*,*,#11719,.T.);
#16313=ORIENTED_EDGE('',*,*,#11708,.T.);
#16314=ORIENTED_EDGE('',*,*,#11705,.F.);
#16315=ORIENTED_EDGE('',*,*,#11720,.T.);
#16316=ORIENTED_EDGE('',*,*,#11721,.F.);
#16317=ORIENTED_EDGE('',*,*,#11722,.F.);
#16318=ORIENTED_EDGE('',*,*,#11717,.F.);
#16319=ORIENTED_EDGE('',*,*,#11711,.T.);
#16320=ORIENTED_EDGE('',*,*,#11709,.T.);
#16321=ORIENTED_EDGE('',*,*,#11719,.F.);
#16322=ORIENTED_EDGE('',*,*,#11715,.F.);
#16323=ORIENTED_EDGE('',*,*,#11723,.F.);
#16324=ORIENTED_EDGE('',*,*,#11720,.F.);
#16325=ORIENTED_EDGE('',*,*,#11704,.F.);
#16326=ORIENTED_EDGE('',*,*,#11722,.T.);
#16327=ORIENTED_EDGE('',*,*,#11724,.F.);
#16328=ORIENTED_EDGE('',*,*,#11713,.F.);
#16329=ORIENTED_EDGE('',*,*,#11716,.T.);
#16330=ORIENTED_EDGE('',*,*,#11714,.T.);
#16331=ORIENTED_EDGE('',*,*,#11724,.T.);
#16332=ORIENTED_EDGE('',*,*,#11721,.T.);
#16333=ORIENTED_EDGE('',*,*,#11723,.T.);
#19160=ADVANCED_FACE('',(#5444),#917,.T.);
#19161=ADVANCED_FACE('',(#5445),#918,.F.);
#19162=ADVANCED_FACE('',(#5446),#919,.T.);
#19163=ADVANCED_FACE('',(#5447),#4587,.T.);
#19164=ADVANCED_FACE('',(#5448),#920,.T.);
#19165=ADVANCED_FACE('',(#5449),#921,.F.);
#19166=ADVANCED_FACE('',(#5450),#922,.T.);
#19167=ADVANCED_FACE('',(#5451),#923,.T.);
#19168=ADVANCED_FACE('',(#5452),#924,.T.);
#19573=CLOSED_SHELL('',(#19160,#19161,#19162,#19163,#19164,#19165,#19166,
#19167,#19168));
#21362=AXIS2_PLACEMENT_3D('',#32335,#26061,#26062);
#21363=AXIS2_PLACEMENT_3D('',#32336,#26063,#26064);
#21364=AXIS2_PLACEMENT_3D('',#32345,#26069,#26070);
#21365=AXIS2_PLACEMENT_3D('',#32351,#26074,#26075);
#21366=AXIS2_PLACEMENT_3D('',#32355,#26077,#26078);
#21367=AXIS2_PLACEMENT_3D('',#32361,#26082,#26083);
#21368=AXIS2_PLACEMENT_3D('',#32366,#26086,#26087);
#21369=AXIS2_PLACEMENT_3D('',#32367,#26088,#26089);
#21370=AXIS2_PLACEMENT_3D('',#32374,#26094,#26095);
#21371=AXIS2_PLACEMENT_3D('',#32375,#26096,#26097);
#21372=AXIS2_PLACEMENT_3D('',#32377,#26099,#26100);
#21373=AXIS2_PLACEMENT_3D('',#32379,#26102,#26103);
#26061=DIRECTION('axis',(0.,0.,1.));
#26062=DIRECTION('refdir',(1.,0.,0.));
#26063=DIRECTION('center_axis',(1.,5.1420277733694E-16,-1.0522467400333E-14));
#26064=DIRECTION('ref_axis',(-1.0522467400333E-14,1.06077175752244E-14,
-1.));
#26065=DIRECTION('',(-1.00001914094642E-12,1.00002200370999E-12,1.));
#26066=DIRECTION('',(-9.47915311079142E-15,-1.,1.E-14));
#26067=DIRECTION('',(1.00001914094642E-12,-9.99999999998997E-13,-1.));
#26068=DIRECTION('',(-9.47915311079142E-15,-1.,1.E-14));
#26069=DIRECTION('center_axis',(-4.5961454925099E-16,1.,6.61092274672771E-17));
#26070=DIRECTION('ref_axis',(-1.05885766278003E-14,6.61092274672722E-17,
-1.));
#26071=DIRECTION('',(1.,-9.54038545074888E-15,9.9999999999998E-15));
#26072=DIRECTION('',(-9.56631913100564E-15,9.99999999999985E-15,1.));
#26073=DIRECTION('',(-1.,9.54038545074888E-15,-9.9999999999998E-15));
#26074=DIRECTION('center_axis',(-1.0522467400333E-14,6.93088260946523E-29,
-1.));
#26075=DIRECTION('ref_axis',(1.,-6.62426369448742E-15,-1.0522467400333E-14));
#26076=DIRECTION('',(-9.47915311079142E-15,-1.,1.E-14));
#26077=DIRECTION('center_axis',(-1.99999999991998E-11,2.E-11,1.));
#26078=DIRECTION('ref_axis',(-1.99995712428458E-11,-1.,1.99999999996E-11));
#26079=DIRECTION('',(1.,-9.99466108488984E-13,9.99906900405741E-13));
#26080=DIRECTION('',(9.99479153109778E-13,1.,-1.00002200371E-12));
#26081=DIRECTION('',(-1.,9.99485333130104E-13,-1.00005108521413E-12));
#26082=DIRECTION('center_axis',(0.,-4.29362650667545E-31,1.));
#26083=DIRECTION('ref_axis',(4.28756753891971E-16,-1.,-4.29362650667545E-31));
#26084=DIRECTION('',(-9.99999999999976E-15,-1.04336808689941E-14,1.));
#26085=DIRECTION('',(-9.56631913100564E-15,9.99999999999985E-15,1.));
#26086=DIRECTION('center_axis',(-1.99999999991998E-11,2.E-11,1.));
#26087=DIRECTION('ref_axis',(-1.99995712428458E-11,-1.,1.99999999996E-11));
#26088=DIRECTION('center_axis',(0.,3.71824206197546E-31,1.));
#26089=DIRECTION('ref_axis',(1.,3.89820370584558E-15,-1.44944649852236E-45));
#26090=DIRECTION('',(-9.47915311079142E-15,-1.,1.E-14));
#26091=DIRECTION('',(1.,-9.99466108488984E-13,9.99906900405741E-13));
#26092=DIRECTION('',(-9.99479153109778E-13,-1.,1.00002200371E-12));
#26093=DIRECTION('',(1.,-9.99466108488984E-13,9.99906900405741E-13));
#26094=DIRECTION('center_axis',(1.,5.2084688920845E-16,-1.0522467400333E-14));
#26095=DIRECTION('ref_axis',(-1.0522467400333E-14,1.01548957588061E-14,
-1.));
#26096=DIRECTION('center_axis',(5.33891510011771E-16,-1.,2.20037109950003E-17));
#26097=DIRECTION('ref_axis',(-1.,-5.33891510011771E-16,1.0522467400333E-14));
#26098=DIRECTION('',(9.99999999998993E-13,-1.00002200370999E-12,-1.));
#26099=DIRECTION('center_axis',(-5.3389151001177E-16,1.,6.61092274672778E-17));
#26100=DIRECTION('ref_axis',(-1.06105803387953E-14,6.61092274672721E-17,
-1.));
#26101=DIRECTION('',(-9.99999999998993E-13,1.00002200370999E-12,1.));
#26102=DIRECTION('center_axis',(1.,5.3389151001188E-16,-1.0522467400333E-14));
#26103=DIRECTION('ref_axis',(-1.0522467400333E-14,1.04954770345521E-14,
-1.));
#32335=CARTESIAN_POINT('',(0.,0.,0.));
#32336=CARTESIAN_POINT('Origin',(0.02115,-0.0223,-0.01175));
#32337=CARTESIAN_POINT('',(0.02115,-0.02545,-0.00525000000000007));
#32338=CARTESIAN_POINT('',(0.02115,-0.02545,-0.00475000000000007));
#32339=CARTESIAN_POINT('',(0.0211500000000101,-0.02545000000001,-0.00849999999999003));
#32340=CARTESIAN_POINT('',(0.02115,-0.0317,-0.00475000000000007));
#32341=CARTESIAN_POINT('',(0.0211500000000101,-0.02545000000001,-0.00474999999999007));
#32342=CARTESIAN_POINT('',(0.02115,-0.0317,-0.00525000000000007));
#32343=CARTESIAN_POINT('',(0.0211500000000101,-0.0317000000000099,-0.00549999999999003));
#32344=CARTESIAN_POINT('',(0.02115000000001,-0.02545000000001,-0.00524999999999007));
#32345=CARTESIAN_POINT('Origin',(0.02115,-0.0317,0.000749999999999928));
#32346=CARTESIAN_POINT('',(0.02065,-0.0317,-0.00475000000000007));
#32347=CARTESIAN_POINT('',(0.0206500000000101,-0.03170000000001,-0.00474999999999007));
#32348=CARTESIAN_POINT('',(0.02065,-0.0317,-0.00525000000000007));
#32349=CARTESIAN_POINT('',(0.0206500000000101,-0.03170000000001,-0.00474999999999007));
#32350=CARTESIAN_POINT('',(0.0206500000000101,-0.03170000000001,-0.00524999999999007));
#32351=CARTESIAN_POINT('Origin',(0.02115,-0.02495,-0.00525000000000007));
#32352=CARTESIAN_POINT('',(0.02065,-0.02545,-0.00525000000000007));
#32353=CARTESIAN_POINT('',(0.0206500000000101,-0.02545000000001,-0.00524999999999007));
#32354=CARTESIAN_POINT('',(0.02115,-0.02495,-0.00525000000000007));
#32355=CARTESIAN_POINT('Origin',(0.02115000000001,-0.02545000000001,-0.00524999999999007));
#32356=CARTESIAN_POINT('',(0.0262,-0.02495,-0.00525000000000013));
#32357=CARTESIAN_POINT('',(0.0229000000000101,-0.02495000000001,-0.00524999999999007));
#32358=CARTESIAN_POINT('',(0.0262,-0.02545,-0.00525000000000013));
#32359=CARTESIAN_POINT('',(0.0262000000000101,-0.02495000000001,-0.00524999999999008));
#32360=CARTESIAN_POINT('',(0.0229000000000101,-0.02545000000001,-0.00524999999999007));
#32361=CARTESIAN_POINT('Origin',(0.02115,-0.02545,-0.00500000000000007));
#32362=CARTESIAN_POINT('',(0.02115,-0.02495,-0.00475000000000007));
#32363=CARTESIAN_POINT('',(0.0211500000000101,-0.02495000000001,-0.00474999999999007));
#32364=CARTESIAN_POINT('',(0.02065,-0.02545,-0.00475000000000007));
#32365=CARTESIAN_POINT('',(0.0206500000000101,-0.02545000000001,-0.00474999999999007));
#32366=CARTESIAN_POINT('Origin',(0.0211500000000101,-0.02545000000001,-0.00474999999999007));
#32367=CARTESIAN_POINT('Origin',(0.02115,-0.02495,-0.00475000000000007));
#32368=CARTESIAN_POINT('',(0.0206500000000101,-0.02545000000001,-0.00474999999999007));
#32369=CARTESIAN_POINT('',(0.0262,-0.02545,-0.00475000000000013));
#32370=CARTESIAN_POINT('',(0.0229000000000101,-0.02545000000001,-0.00474999999999007));
#32371=CARTESIAN_POINT('',(0.0262,-0.02495,-0.00475000000000013));
#32372=CARTESIAN_POINT('',(0.0262000000000101,-0.02545000000001,-0.00474999999999008));
#32373=CARTESIAN_POINT('',(0.0229000000000101,-0.02495000000001,-0.00474999999999007));
#32374=CARTESIAN_POINT('Origin',(0.02065,-0.02545,-0.00475000000000007));
#32375=CARTESIAN_POINT('Origin',(0.0229,-0.02545,-0.00475000000000009));
#32376=CARTESIAN_POINT('',(0.0262000000000101,-0.02545000000001,-0.00524999999999008));
#32377=CARTESIAN_POINT('Origin',(0.0229,-0.02495,-0.00525000000000009));
#32378=CARTESIAN_POINT('',(0.0262000000000101,-0.02495000000001,-0.00474999999999008));
#32379=CARTESIAN_POINT('Origin',(0.0262,-0.0252,-0.00500000000000013));
#34827=UNCERTAINTY_MEASURE_WITH_UNIT(LENGTH_MEASURE(1.E-5),#34877,
'DISTANCE_ACCURACY_VALUE',
'Maximum model space distance between geometric entities at asserted c
onnectivities');
#34841=UNCERTAINTY_MEASURE_WITH_UNIT(LENGTH_MEASURE(1.E-5),#34877,
'DISTANCE_ACCURACY_VALUE',
'Maximum model space distance between geometric entities at asserted c
onnectivities');
#34862=(
GEOMETRIC_REPRESENTATION_CONTEXT(3)
GLOBAL_UNCERTAINTY_ASSIGNED_CONTEXT((#34827))
GLOBAL_UNIT_ASSIGNED_CONTEXT((#34877,#34878,#34879))
REPRESENTATION_CONTEXT('','3D')
);
#34876=(
GEOMETRIC_REPRESENTATION_CONTEXT(3)
GLOBAL_UNCERTAINTY_ASSIGNED_CONTEXT((#34841))
GLOBAL_UNIT_ASSIGNED_CONTEXT((#34877,#34878,#34879))
REPRESENTATION_CONTEXT('','3D')
);
#34877=(
LENGTH_UNIT()
NAMED_UNIT(*)
SI_UNIT($,.METRE.)
);
#34878=(
NAMED_UNIT(*)
PLANE_ANGLE_UNIT()
SI_UNIT($,.RADIAN.)
);
#34879=(
NAMED_UNIT(*)
SI_UNIT($,.STERADIAN.)
SOLID_ANGLE_UNIT()
);
#34900=SHAPE_DEFINITION_REPRESENTATION(#34934,#35004);
#34934=PRODUCT_DEFINITION_SHAPE('',$,#35039);
#35004=SHAPE_REPRESENTATION('',(#21362),#34862);
#35018=PRODUCT_DEFINITION_CONTEXT('part definition',#35122,'design');
#35039=PRODUCT_DEFINITION('Socket Screw 4','Socket Screw 4',#35073,#35018);
#35073=PRODUCT_DEFINITION_FORMATION('',$,#35144);
#35122=APPLICATION_CONTEXT('Managed model based 3d engineering');
#35123=PRODUCT_CONTEXT('part definition',#35122,'mechanical');
#35144=PRODUCT('Socket Screw 4','Socket Screw 4',
'LEGAL AND USAGE DISCLAIMER: this Data/Model is provided \X2\201C\X0\A
S IS\X2\201D\X0\ for informational and representational only. It is a 
geometric approximation and is NOT engineered, certified, or guarantee
d for dimensional accuracy, exact tolerances, or production-level prec
ision. Vendor disclaims all implied warranties including fitness for a
 particular purpose. DO NOT USE FOR DIRECT PHYSICAL MANUFACTURING, AUT
OMATED PRODUCTION, OR SAFETY-CRITICAL SYSTEMS without independent engi
neering verification and resolution of any design discrepancies.',(#35123));
#35166=PRESENTATION_STYLE_ASSIGNMENT((#35175));
#35175=SURFACE_STYLE_USAGE(.BOTH.,#35184);
#35184=SURFACE_SIDE_STYLE('',(#35193));
#35193=SURFACE_STYLE_FILL_AREA(#35202);
#35202=FILL_AREA_STYLE('Paint - Enamel Glossy (Grey)',(#35211));
#35211=FILL_AREA_STYLE_COLOUR('Paint - Enamel Glossy (Grey)',#35220);
#35220=COLOUR_RGB('Paint - Enamel Glossy (Grey)',0.701960784313725,0.701960784313725,
0.701960784313725);
ENDSEC;
END-ISO-10303-21;
